ISO-10303-21;
HEADER;
/* Generated by software containing ST-Developer
 * from STEP Tools, Inc. (www.steptools.com) 
 */

FILE_DESCRIPTION(
/* description */ ('Pedal-braked fixed caster'),
/* implementation_level */ '2;1');

FILE_NAME(
/* name */ 'M4x10 Cap Screw.step',
/* time_stamp */ '2026-10-28T03:26:52-07:00',
/* author */ (''),
/* organization */ (''),
/* preprocessor_version */ 'ST-DEVELOPER v20.2',
/* originating_system */ 'Autodesk Translation Framework v15.17.0.0',
/* authorisation */ '');

FILE_SCHEMA (('AUTOMOTIVE_DESIGN { 1 0 10303 214 3 1 1 }'));
ENDSEC;

DATA;
#10=MECHANICAL_DESIGN_GEOMETRIC_PRESENTATION_REPRESENTATION('',(#210),#5734);
#159=CONICAL_SURFACE('',#3306,0.325,0.785398163397448);
#160=CONICAL_SURFACE('',#3310,0.335,0.785398163397448);
#161=CONICAL_SURFACE('',#3314,0.21,0.463647609000806);
#170=ORIENTED_CLOSED_SHELL('',*,#2991,.F.);
#171=BREP_WITH_VOIDS('Body1',#2992,(#170));
#176=SHAPE_REPRESENTATION_RELATIONSHIP('SRR','None',#5814,#193);
#193=ADVANCED_BREP_SHAPE_REPRESENTATION('',(#171),#5718);
#210=STYLED_ITEM('',(#5991),#171);
#268=CYLINDRICAL_SURFACE('',#3308,0.35);
#269=CYLINDRICAL_SURFACE('',#3316,0.1954);
#317=FACE_BOUND('',#747,.T.);
#370=CIRCLE('',#3303,0.1954);
#371=CIRCLE('',#3305,0.3);
#372=CIRCLE('',#3307,0.35);
#373=CIRCLE('',#3309,0.35);
#374=CIRCLE('',#3311,0.32);
#375=CIRCLE('',#3313,0.22);
#376=CIRCLE('',#3315,0.1954);
#533=FACE_OUTER_BOUND('',#733,.T.);
#534=FACE_OUTER_BOUND('',#734,.T.);
#535=FACE_OUTER_BOUND('',#735,.T.);
#536=FACE_OUTER_BOUND('',#736,.T.);
#537=FACE_OUTER_BOUND('',#737,.T.);
#538=FACE_OUTER_BOUND('',#738,.T.);
#539=FACE_OUTER_BOUND('',#739,.T.);
#540=FACE_OUTER_BOUND('',#740,.T.);
#541=FACE_OUTER_BOUND('',#741,.T.);
#542=FACE_OUTER_BOUND('',#742,.T.);
#543=FACE_OUTER_BOUND('',#743,.T.);
#544=FACE_OUTER_BOUND('',#744,.T.);
#545=FACE_OUTER_BOUND('',#745,.T.);
#546=FACE_OUTER_BOUND('',#746,.T.);
#547=FACE_OUTER_BOUND('',#748,.T.);
#548=FACE_OUTER_BOUND('',#749,.T.);
#733=EDGE_LOOP('',(#2210,#2211,#2212,#2213));
#734=EDGE_LOOP('',(#2214,#2215,#2216,#2217));
#735=EDGE_LOOP('',(#2218,#2219,#2220,#2221));
#736=EDGE_LOOP('',(#2222,#2223,#2224,#2225));
#737=EDGE_LOOP('',(#2226,#2227,#2228,#2229));
#738=EDGE_LOOP('',(#2230,#2231,#2232,#2233));
#739=EDGE_LOOP('',(#2234,#2235,#2236,#2237,#2238,#2239));
#740=EDGE_LOOP('',(#2240,#2241,#2242,#2243,#2244,#2245));
#741=EDGE_LOOP('',(#2246));
#742=EDGE_LOOP('',(#2247));
#743=EDGE_LOOP('',(#2248,#2249,#2250,#2251));
#744=EDGE_LOOP('',(#2252,#2253,#2254,#2255));
#745=EDGE_LOOP('',(#2256,#2257,#2258,#2259));
#746=EDGE_LOOP('',(#2260));
#747=EDGE_LOOP('',(#2261));
#748=EDGE_LOOP('',(#2262,#2263,#2264,#2265));
#749=EDGE_LOOP('',(#2266,#2267,#2268,#2269));
#982=LINE('',#4787,#1194);
#983=LINE('',#4789,#1195);
#984=LINE('',#4791,#1196);
#985=LINE('',#4792,#1197);
#986=LINE('',#4795,#1198);
#987=LINE('',#4797,#1199);
#988=LINE('',#4798,#1200);
#989=LINE('',#4801,#1201);
#990=LINE('',#4803,#1202);
#991=LINE('',#4804,#1203);
#992=LINE('',#4807,#1204);
#993=LINE('',#4809,#1205);
#994=LINE('',#4810,#1206);
#995=LINE('',#4813,#1207);
#996=LINE('',#4815,#1208);
#997=LINE('',#4816,#1209);
#998=LINE('',#4818,#1210);
#999=LINE('',#4819,#1211);
#1000=LINE('',#4831,#1212);
#1001=LINE('',#4835,#1213);
#1002=LINE('',#4839,#1214);
#1003=LINE('',#4846,#1215);
#1004=LINE('',#4848,#1216);
#1194=VECTOR('',#3856,1.);
#1195=VECTOR('',#3857,1.);
#1196=VECTOR('',#3858,1.);
#1197=VECTOR('',#3859,1.);
#1198=VECTOR('',#3862,1.);
#1199=VECTOR('',#3863,1.);
#1200=VECTOR('',#3864,1.);
#1201=VECTOR('',#3867,1.);
#1202=VECTOR('',#3868,1.);
#1203=VECTOR('',#3869,1.);
#1204=VECTOR('',#3872,1.);
#1205=VECTOR('',#3873,1.);
#1206=VECTOR('',#3874,1.);
#1207=VECTOR('',#3877,1.);
#1208=VECTOR('',#3878,1.);
#1209=VECTOR('',#3879,1.);
#1210=VECTOR('',#3882,1.);
#1211=VECTOR('',#3883,1.);
#1212=VECTOR('',#3900,0.325);
#1213=VECTOR('',#3905,0.35);
#1214=VECTOR('',#3910,0.335);
#1215=VECTOR('',#3919,0.21);
#1216=VECTOR('',#3922,0.2);
#1391=VERTEX_POINT('',#4785);
#1392=VERTEX_POINT('',#4786);
#1393=VERTEX_POINT('',#4788);
#1394=VERTEX_POINT('',#4790);
#1395=VERTEX_POINT('',#4794);
#1396=VERTEX_POINT('',#4796);
#1397=VERTEX_POINT('',#4800);
#1398=VERTEX_POINT('',#4802);
#1399=VERTEX_POINT('',#4806);
#1400=VERTEX_POINT('',#4808);
#1401=VERTEX_POINT('',#4812);
#1402=VERTEX_POINT('',#4814);
#1403=VERTEX_POINT('',#4823);
#1404=VERTEX_POINT('',#4826);
#1405=VERTEX_POINT('',#4829);
#1406=VERTEX_POINT('',#4833);
#1407=VERTEX_POINT('',#4837);
#1408=VERTEX_POINT('',#4841);
#1409=VERTEX_POINT('',#4844);
#1695=EDGE_CURVE('',#1391,#1392,#982,.T.);
#1696=EDGE_CURVE('',#1392,#1393,#983,.T.);
#1697=EDGE_CURVE('',#1393,#1394,#984,.T.);
#1698=EDGE_CURVE('',#1391,#1394,#985,.T.);
#1699=EDGE_CURVE('',#1392,#1395,#986,.T.);
#1700=EDGE_CURVE('',#1395,#1396,#987,.T.);
#1701=EDGE_CURVE('',#1396,#1393,#988,.T.);
#1702=EDGE_CURVE('',#1395,#1397,#989,.T.);
#1703=EDGE_CURVE('',#1397,#1398,#990,.T.);
#1704=EDGE_CURVE('',#1398,#1396,#991,.T.);
#1705=EDGE_CURVE('',#1397,#1399,#992,.T.);
#1706=EDGE_CURVE('',#1399,#1400,#993,.T.);
#1707=EDGE_CURVE('',#1400,#1398,#994,.T.);
#1708=EDGE_CURVE('',#1399,#1401,#995,.T.);
#1709=EDGE_CURVE('',#1401,#1402,#996,.T.);
#1710=EDGE_CURVE('',#1402,#1400,#997,.T.);
#1711=EDGE_CURVE('',#1401,#1391,#998,.T.);
#1712=EDGE_CURVE('',#1394,#1402,#999,.T.);
#1713=EDGE_CURVE('',#1403,#1403,#370,.T.);
#1714=EDGE_CURVE('',#1404,#1404,#371,.T.);
#1715=EDGE_CURVE('',#1405,#1405,#372,.T.);
#1716=EDGE_CURVE('',#1405,#1404,#1000,.T.);
#1717=EDGE_CURVE('',#1406,#1406,#373,.T.);
#1718=EDGE_CURVE('',#1406,#1405,#1001,.T.);
#1719=EDGE_CURVE('',#1407,#1407,#374,.T.);
#1720=EDGE_CURVE('',#1407,#1406,#1002,.T.);
#1721=EDGE_CURVE('',#1408,#1408,#375,.T.);
#1722=EDGE_CURVE('',#1409,#1409,#376,.F.);
#1723=EDGE_CURVE('',#1409,#1408,#1003,.T.);
#1724=EDGE_CURVE('',#1403,#1409,#1004,.T.);
#2210=ORIENTED_EDGE('',*,*,#1695,.T.);
#2211=ORIENTED_EDGE('',*,*,#1696,.T.);
#2212=ORIENTED_EDGE('',*,*,#1697,.T.);
#2213=ORIENTED_EDGE('',*,*,#1698,.F.);
#2214=ORIENTED_EDGE('',*,*,#1699,.T.);
#2215=ORIENTED_EDGE('',*,*,#1700,.T.);
#2216=ORIENTED_EDGE('',*,*,#1701,.T.);
#2217=ORIENTED_EDGE('',*,*,#1696,.F.);
#2218=ORIENTED_EDGE('',*,*,#1702,.T.);
#2219=ORIENTED_EDGE('',*,*,#1703,.T.);
#2220=ORIENTED_EDGE('',*,*,#1704,.T.);
#2221=ORIENTED_EDGE('',*,*,#1700,.F.);
#2222=ORIENTED_EDGE('',*,*,#1705,.T.);
#2223=ORIENTED_EDGE('',*,*,#1706,.T.);
#2224=ORIENTED_EDGE('',*,*,#1707,.T.);
#2225=ORIENTED_EDGE('',*,*,#1703,.F.);
#2226=ORIENTED_EDGE('',*,*,#1708,.T.);
#2227=ORIENTED_EDGE('',*,*,#1709,.T.);
#2228=ORIENTED_EDGE('',*,*,#1710,.T.);
#2229=ORIENTED_EDGE('',*,*,#1706,.F.);
#2230=ORIENTED_EDGE('',*,*,#1711,.T.);
#2231=ORIENTED_EDGE('',*,*,#1698,.T.);
#2232=ORIENTED_EDGE('',*,*,#1712,.T.);
#2233=ORIENTED_EDGE('',*,*,#1709,.F.);
#2234=ORIENTED_EDGE('',*,*,#1711,.F.);
#2235=ORIENTED_EDGE('',*,*,#1708,.F.);
#2236=ORIENTED_EDGE('',*,*,#1705,.F.);
#2237=ORIENTED_EDGE('',*,*,#1702,.F.);
#2238=ORIENTED_EDGE('',*,*,#1699,.F.);
#2239=ORIENTED_EDGE('',*,*,#1695,.F.);
#2240=ORIENTED_EDGE('',*,*,#1712,.F.);
#2241=ORIENTED_EDGE('',*,*,#1697,.F.);
#2242=ORIENTED_EDGE('',*,*,#1701,.F.);
#2243=ORIENTED_EDGE('',*,*,#1704,.F.);
#2244=ORIENTED_EDGE('',*,*,#1707,.F.);
#2245=ORIENTED_EDGE('',*,*,#1710,.F.);
#2246=ORIENTED_EDGE('',*,*,#1713,.F.);
#2247=ORIENTED_EDGE('',*,*,#1714,.F.);
#2248=ORIENTED_EDGE('',*,*,#1715,.F.);
#2249=ORIENTED_EDGE('',*,*,#1716,.T.);
#2250=ORIENTED_EDGE('',*,*,#1714,.T.);
#2251=ORIENTED_EDGE('',*,*,#1716,.F.);
#2252=ORIENTED_EDGE('',*,*,#1717,.F.);
#2253=ORIENTED_EDGE('',*,*,#1718,.T.);
#2254=ORIENTED_EDGE('',*,*,#1715,.T.);
#2255=ORIENTED_EDGE('',*,*,#1718,.F.);
#2256=ORIENTED_EDGE('',*,*,#1719,.F.);
#2257=ORIENTED_EDGE('',*,*,#1720,.T.);
#2258=ORIENTED_EDGE('',*,*,#1717,.T.);
#2259=ORIENTED_EDGE('',*,*,#1720,.F.);
#2260=ORIENTED_EDGE('',*,*,#1719,.T.);
#2261=ORIENTED_EDGE('',*,*,#1721,.F.);
#2262=ORIENTED_EDGE('',*,*,#1722,.F.);
#2263=ORIENTED_EDGE('',*,*,#1723,.T.);
#2264=ORIENTED_EDGE('',*,*,#1721,.T.);
#2265=ORIENTED_EDGE('',*,*,#1723,.F.);
#2266=ORIENTED_EDGE('',*,*,#1713,.T.);
#2267=ORIENTED_EDGE('',*,*,#1724,.T.);
#2268=ORIENTED_EDGE('',*,*,#1722,.T.);
#2269=ORIENTED_EDGE('',*,*,#1724,.F.);
#2742=PLANE('',#3294);
#2743=PLANE('',#3295);
#2744=PLANE('',#3296);
#2745=PLANE('',#3297);
#2746=PLANE('',#3298);
#2747=PLANE('',#3299);
#2748=PLANE('',#3300);
#2749=PLANE('',#3301);
#2750=PLANE('',#3302);
#2751=PLANE('',#3304);
#2752=PLANE('',#3312);
#2866=ADVANCED_FACE('',(#533),#2742,.F.);
#2867=ADVANCED_FACE('',(#534),#2743,.F.);
#2868=ADVANCED_FACE('',(#535),#2744,.F.);
#2869=ADVANCED_FACE('',(#536),#2745,.F.);
#2870=ADVANCED_FACE('',(#537),#2746,.F.);
#2871=ADVANCED_FACE('',(#538),#2747,.F.);
#2872=ADVANCED_FACE('',(#539),#2748,.F.);
#2873=ADVANCED_FACE('',(#540),#2749,.F.);
#2874=ADVANCED_FACE('',(#541),#2750,.F.);
#2875=ADVANCED_FACE('',(#542),#2751,.T.);
#2876=ADVANCED_FACE('',(#543),#159,.T.);
#2877=ADVANCED_FACE('',(#544),#268,.T.);
#2878=ADVANCED_FACE('',(#545),#160,.T.);
#2879=ADVANCED_FACE('',(#546,#317),#2752,.T.);
#2880=ADVANCED_FACE('',(#547),#161,.T.);
#2881=ADVANCED_FACE('',(#548),#269,.T.);
#2991=CLOSED_SHELL('',(#2866,#2867,#2868,#2869,#2870,#2871,#2872,#2873));
#2992=CLOSED_SHELL('',(#2874,#2875,#2876,#2877,#2878,#2879,#2880,#2881));
#3293=AXIS2_PLACEMENT_3D('',#4783,#3852,#3853);
#3294=AXIS2_PLACEMENT_3D('',#4784,#3854,#3855);
#3295=AXIS2_PLACEMENT_3D('',#4793,#3860,#3861);
#3296=AXIS2_PLACEMENT_3D('',#4799,#3865,#3866);
#3297=AXIS2_PLACEMENT_3D('',#4805,#3870,#3871);
#3298=AXIS2_PLACEMENT_3D('',#4811,#3875,#3876);
#3299=AXIS2_PLACEMENT_3D('',#4817,#3880,#3881);
#3300=AXIS2_PLACEMENT_3D('',#4820,#3884,#3885);
#3301=AXIS2_PLACEMENT_3D('',#4821,#3886,#3887);
#3302=AXIS2_PLACEMENT_3D('',#4822,#3888,#3889);
#3303=AXIS2_PLACEMENT_3D('',#4824,#3890,#3891);
#3304=AXIS2_PLACEMENT_3D('',#4825,#3892,#3893);
#3305=AXIS2_PLACEMENT_3D('',#4827,#3894,#3895);
#3306=AXIS2_PLACEMENT_3D('',#4828,#3896,#3897);
#3307=AXIS2_PLACEMENT_3D('',#4830,#3898,#3899);
#3308=AXIS2_PLACEMENT_3D('',#4832,#3901,#3902);
#3309=AXIS2_PLACEMENT_3D('',#4834,#3903,#3904);
#3310=AXIS2_PLACEMENT_3D('',#4836,#3906,#3907);
#3311=AXIS2_PLACEMENT_3D('',#4838,#3908,#3909);
#3312=AXIS2_PLACEMENT_3D('',#4840,#3911,#3912);
#3313=AXIS2_PLACEMENT_3D('',#4842,#3913,#3914);
#3314=AXIS2_PLACEMENT_3D('',#4843,#3915,#3916);
#3315=AXIS2_PLACEMENT_3D('',#4845,#3917,#3918);
#3316=AXIS2_PLACEMENT_3D('',#4847,#3920,#3921);
#3852=DIRECTION('axis',(0.,0.,1.));
#3853=DIRECTION('refdir',(1.,0.,0.));
#3854=DIRECTION('center_axis',(0.866025403784439,0.,-0.5));
#3855=DIRECTION('ref_axis',(0.5,0.,0.866025403784439));
#3856=DIRECTION('',(-0.5,0.,-0.866025403784439));
#3857=DIRECTION('',(0.,-1.,0.));
#3858=DIRECTION('',(0.5,0.,0.866025403784439));
#3859=DIRECTION('',(0.,-1.,0.));
#3860=DIRECTION('center_axis',(1.60246890531964E-16,0.,-1.));
#3861=DIRECTION('ref_axis',(1.,0.,1.60246890531964E-16));
#3862=DIRECTION('',(-1.,0.,-1.60246890531964E-16));
#3863=DIRECTION('',(0.,-1.,0.));
#3864=DIRECTION('',(1.,0.,1.60246890531964E-16));
#3865=DIRECTION('center_axis',(-0.866025403784439,0.,-0.5));
#3866=DIRECTION('ref_axis',(0.5,0.,-0.866025403784439));
#3867=DIRECTION('',(-0.5,0.,0.866025403784439));
#3868=DIRECTION('',(0.,-1.,0.));
#3869=DIRECTION('',(0.5,0.,-0.866025403784439));
#3870=DIRECTION('center_axis',(-0.866025403784439,0.,0.5));
#3871=DIRECTION('ref_axis',(-0.5,0.,-0.866025403784439));
#3872=DIRECTION('',(0.5,0.,0.866025403784439));
#3873=DIRECTION('',(0.,-1.,0.));
#3874=DIRECTION('',(-0.5,0.,-0.866025403784439));
#3875=DIRECTION('center_axis',(-1.60246890531964E-16,0.,1.));
#3876=DIRECTION('ref_axis',(-1.,0.,-1.60246890531964E-16));
#3877=DIRECTION('',(1.,0.,1.60246890531964E-16));
#3878=DIRECTION('',(0.,-1.,0.));
#3879=DIRECTION('',(-1.,0.,-1.60246890531964E-16));
#3880=DIRECTION('center_axis',(0.866025403784439,0.,0.5));
#3881=DIRECTION('ref_axis',(-0.5,0.,0.866025403784439));
#3882=DIRECTION('',(0.5,0.,-0.866025403784439));
#3883=DIRECTION('',(-0.5,0.,0.866025403784439));
#3884=DIRECTION('center_axis',(0.,1.,0.));
#3885=DIRECTION('ref_axis',(1.,0.,0.));
#3886=DIRECTION('center_axis',(0.,-1.,0.));
#3887=DIRECTION('ref_axis',(0.,0.,-1.));
#3888=DIRECTION('center_axis',(0.,1.,0.));
#3889=DIRECTION('ref_axis',(1.,0.,0.));
#3890=DIRECTION('center_axis',(0.,1.,0.));
#3891=DIRECTION('ref_axis',(1.,0.,0.));
#3892=DIRECTION('center_axis',(0.,1.,0.));
#3893=DIRECTION('ref_axis',(0.,0.,1.));
#3894=DIRECTION('center_axis',(0.,-1.,0.));
#3895=DIRECTION('ref_axis',(1.,0.,0.));
#3896=DIRECTION('center_axis',(0.,-1.,0.));
#3897=DIRECTION('ref_axis',(1.,0.,0.));
#3898=DIRECTION('center_axis',(0.,-1.,0.));
#3899=DIRECTION('ref_axis',(1.,0.,0.));
#3900=DIRECTION('',(0.707106781186547,0.707106781186548,8.65956056235493E-17));
#3901=DIRECTION('center_axis',(0.,-1.,0.));
#3902=DIRECTION('ref_axis',(1.,0.,0.));
#3903=DIRECTION('center_axis',(0.,-1.,0.));
#3904=DIRECTION('ref_axis',(1.,0.,0.));
#3905=DIRECTION('',(0.,1.,0.));
#3906=DIRECTION('center_axis',(0.,1.,0.));
#3907=DIRECTION('ref_axis',(1.,0.,0.));
#3908=DIRECTION('center_axis',(0.,-1.,0.));
#3909=DIRECTION('ref_axis',(1.,0.,0.));
#3910=DIRECTION('',(-0.707106781186547,0.707106781186548,-8.65956056235493E-17));
#3911=DIRECTION('center_axis',(0.,-1.,0.));
#3912=DIRECTION('ref_axis',(0.,0.,-1.));
#3913=DIRECTION('center_axis',(0.,-1.,0.));
#3914=DIRECTION('ref_axis',(1.,0.,0.));
#3915=DIRECTION('center_axis',(0.,1.,0.));
#3916=DIRECTION('ref_axis',(1.,0.,0.));
#3917=DIRECTION('center_axis',(0.,1.,0.));
#3918=DIRECTION('ref_axis',(1.,0.,0.));
#3919=DIRECTION('',(-0.447213595499958,0.894427190999916,-5.47678698264203E-17));
#3920=DIRECTION('center_axis',(0.,-1.,0.));
#3921=DIRECTION('ref_axis',(1.,0.,0.));
#3922=DIRECTION('',(0.,1.,0.));
#4783=CARTESIAN_POINT('',(0.,0.,0.));
#4784=CARTESIAN_POINT('Origin',(0.0866025403784439,-0.4,-0.15));
#4785=CARTESIAN_POINT('',(0.173205080756888,-0.4,0.));
#4786=CARTESIAN_POINT('',(0.0866025403784439,-0.4,-0.15));
#4787=CARTESIAN_POINT('',(0.173205080756888,-0.4,0.));
#4788=CARTESIAN_POINT('',(0.0866025403784439,-0.64,-0.15));
#4789=CARTESIAN_POINT('',(0.0866025403784439,-0.4,-0.15));
#4790=CARTESIAN_POINT('',(0.173205080756888,-0.64,0.));
#4791=CARTESIAN_POINT('',(0.173205080756888,-0.64,0.));
#4792=CARTESIAN_POINT('',(0.173205080756888,-0.4,0.));
#4793=CARTESIAN_POINT('Origin',(-0.0866025403784438,-0.4,-0.15));
#4794=CARTESIAN_POINT('',(-0.0866025403784438,-0.4,-0.15));
#4795=CARTESIAN_POINT('',(0.0866025403784439,-0.4,-0.15));
#4796=CARTESIAN_POINT('',(-0.0866025403784438,-0.64,-0.15));
#4797=CARTESIAN_POINT('',(-0.0866025403784438,-0.4,-0.15));
#4798=CARTESIAN_POINT('',(0.0866025403784439,-0.64,-0.15));
#4799=CARTESIAN_POINT('Origin',(-0.173205080756888,-0.4,-2.77555756156289E-17));
#4800=CARTESIAN_POINT('',(-0.173205080756888,-0.4,-2.12115047744981E-17));
#4801=CARTESIAN_POINT('',(-0.0866025403784438,-0.4,-0.15));
#4802=CARTESIAN_POINT('',(-0.173205080756888,-0.64,-2.77555756156289E-17));
#4803=CARTESIAN_POINT('',(-0.173205080756888,-0.4,-2.12115047744981E-17));
#4804=CARTESIAN_POINT('',(-0.0866025403784438,-0.64,-0.15));
#4805=CARTESIAN_POINT('Origin',(-0.0866025403784439,-0.4,0.15));
#4806=CARTESIAN_POINT('',(-0.0866025403784439,-0.4,0.15));
#4807=CARTESIAN_POINT('',(-0.173205080756888,-0.4,-2.12115047744981E-17));
#4808=CARTESIAN_POINT('',(-0.0866025403784439,-0.64,0.15));
#4809=CARTESIAN_POINT('',(-0.0866025403784439,-0.4,0.15));
#4810=CARTESIAN_POINT('',(-0.173205080756888,-0.64,-2.12115047744981E-17));
#4811=CARTESIAN_POINT('Origin',(0.0866025403784439,-0.4,0.15));
#4812=CARTESIAN_POINT('',(0.0866025403784439,-0.4,0.15));
#4813=CARTESIAN_POINT('',(-0.0866025403784439,-0.4,0.15));
#4814=CARTESIAN_POINT('',(0.0866025403784439,-0.64,0.15));
#4815=CARTESIAN_POINT('',(0.0866025403784439,-0.4,0.15));
#4816=CARTESIAN_POINT('',(-0.0866025403784439,-0.64,0.15));
#4817=CARTESIAN_POINT('Origin',(0.173205080756888,-0.4,0.));
#4818=CARTESIAN_POINT('',(0.0866025403784439,-0.4,0.15));
#4819=CARTESIAN_POINT('',(0.0866025403784439,-0.64,0.15));
#4820=CARTESIAN_POINT('Origin',(0.,-0.4,-2.77555756156289E-17));
#4821=CARTESIAN_POINT('Origin',(0.,-0.64,-2.77555756156289E-17));
#4822=CARTESIAN_POINT('Origin',(0.,-1.,0.));
#4823=CARTESIAN_POINT('',(-0.1954,-1.,2.39295984553393E-17));
#4824=CARTESIAN_POINT('Origin',(0.,-1.,0.));
#4825=CARTESIAN_POINT('Origin',(0.3,0.4,0.));
#4826=CARTESIAN_POINT('',(-0.3,0.4,-3.67394039744206E-17));
#4827=CARTESIAN_POINT('Origin',(0.,0.4,0.));
#4828=CARTESIAN_POINT('Origin',(0.,0.375,0.));
#4829=CARTESIAN_POINT('',(-0.35,0.35,-4.28626379701573E-17));
#4830=CARTESIAN_POINT('Origin',(0.,0.35,0.));
#4831=CARTESIAN_POINT('',(-0.325,0.375,-3.9801020972289E-17));
#4832=CARTESIAN_POINT('Origin',(0.,0.19,0.));
#4833=CARTESIAN_POINT('',(-0.35,0.03,-4.28626379701574E-17));
#4834=CARTESIAN_POINT('Origin',(0.,0.03,0.));
#4835=CARTESIAN_POINT('',(-0.35,0.19,-4.28626379701574E-17));
#4836=CARTESIAN_POINT('Origin',(0.,0.0149999999999999,0.));
#4837=CARTESIAN_POINT('',(-0.32,-3.29597460435593E-17,-3.91886975727153E-17));
#4838=CARTESIAN_POINT('Origin',(0.,0.,0.));
#4839=CARTESIAN_POINT('',(-0.335,0.0149999999999999,-4.10256677714363E-17));
#4840=CARTESIAN_POINT('Origin',(0.22,0.,0.));
#4841=CARTESIAN_POINT('',(-0.22,-6.93889390390723E-18,-2.69422295812418E-17));
#4842=CARTESIAN_POINT('Origin',(0.,0.,0.));
#4843=CARTESIAN_POINT('Origin',(0.,-0.02,0.));
#4844=CARTESIAN_POINT('',(-0.1954,-0.0492,2.39295984553393E-17));
#4845=CARTESIAN_POINT('Origin',(0.,-0.0492,0.));
#4846=CARTESIAN_POINT('',(-0.21,-0.02,-2.57175827820944E-17));
#4847=CARTESIAN_POINT('Origin',(0.,-0.8,0.));
#4848=CARTESIAN_POINT('',(-0.1954,-0.8,-2.39295984553393E-17));
#5695=UNCERTAINTY_MEASURE_WITH_UNIT(LENGTH_MEASURE(0.001),#5735,
'DISTANCE_ACCURACY_VALUE',
'Maximum model space distance between geometric entities at asserted c
onnectivities');
#5711=UNCERTAINTY_MEASURE_WITH_UNIT(LENGTH_MEASURE(0.001),#5735,
'DISTANCE_ACCURACY_VALUE',
'Maximum model space distance between geometric entities at asserted c
onnectivities');
#5718=(
GEOMETRIC_REPRESENTATION_CONTEXT(3)
GLOBAL_UNCERTAINTY_ASSIGNED_CONTEXT((#5695))
GLOBAL_UNIT_ASSIGNED_CONTEXT((#5735,#5737,#5738))
REPRESENTATION_CONTEXT('','3D')
);
#5734=(
GEOMETRIC_REPRESENTATION_CONTEXT(3)
GLOBAL_UNCERTAINTY_ASSIGNED_CONTEXT((#5711))
GLOBAL_UNIT_ASSIGNED_CONTEXT((#5735,#5737,#5738))
REPRESENTATION_CONTEXT('','3D')
);
#5735=(
LENGTH_UNIT()
NAMED_UNIT(*)
SI_UNIT(.CENTI.,.METRE.)
);
#5737=(
NAMED_UNIT(*)
PLANE_ANGLE_UNIT()
SI_UNIT($,.RADIAN.)
);
#5738=(
NAMED_UNIT(*)
SI_UNIT($,.STERADIAN.)
SOLID_ANGLE_UNIT()
);
#5745=SHAPE_DEFINITION_REPRESENTATION(#5767,#5814);
#5767=PRODUCT_DEFINITION_SHAPE('',$,#5837);
#5814=SHAPE_REPRESENTATION('',(#3293),#5718);
#5830=PRODUCT_DEFINITION_CONTEXT('part definition',#5898,'design');
#5837=PRODUCT_DEFINITION('M4x10 Cap Screw','M4x10 Cap Screw',#5859,#5830);
#5859=PRODUCT_DEFINITION_FORMATION('',$,#5906);
#5898=APPLICATION_CONTEXT(
'Core Data for Automotive Mechanical Design Process');
#5899=PRODUCT_CONTEXT('part definition',#5898,'mechanical');
#5906=PRODUCT('M4x10 Cap Screw','M4x10 Cap Screw','M4x10 Cap Screw',(#5899));
#5985=COLOUR_RGB('Black',0.12,0.14,0.17);
#5986=FILL_AREA_STYLE_COLOUR('',#5985);
#5987=FILL_AREA_STYLE('',(#5986));
#5988=SURFACE_STYLE_FILL_AREA(#5987);
#5989=SURFACE_SIDE_STYLE('',(#5988));
#5990=SURFACE_STYLE_USAGE(.BOTH.,#5989);
#5991=PRESENTATION_STYLE_ASSIGNMENT((#5990));
ENDSEC;
END-ISO-10303-21;
